ISO-10303-21;
HEADER;
/* Generated by software containing ST-Developer
 * from STEP Tools, Inc. (www.steptools.com) 
 */

FILE_DESCRIPTION(
/* description */ (''),
/* implementation_level */ '2;1');

FILE_NAME(
/* name */ 'M5x14 Steel 4.6 Plain v1.step',
/* time_stamp */ '2026-10-23T22:29:29+06:00',
/* author */ (''),
/* organization */ (''),
/* preprocessor_version */ 'ST-DEVELOPER v20.2',
/* originating_system */ 'Autodesk Translation Framework v15.15.0.0',
/* authorisation */ '');

FILE_SCHEMA (('AUTOMOTIVE_DESIGN { 1 0 10303 214 3 1 1 }'));
ENDSEC;

DATA;
#10=MECHANICAL_DESIGN_GEOMETRIC_PRESENTATION_REPRESENTATION('',(#72),#7047);
#52=SHAPE_REPRESENTATION_RELATIONSHIP('SRR','None',#7085,#62);
#62=ADVANCED_BREP_SHAPE_REPRESENTATION('',(#85),#7037);
#72=STYLED_ITEM('',(#7212),#85);
#85=MANIFOLD_SOLID_BREP('Body1',#3397);
#95=SPHERICAL_SURFACE('',#3575,12.8319377609308);
#99=CONICAL_SURFACE('',#3570,2.33923048454133,0.261799387799147);
#100=CONICAL_SURFACE('',#3579,5.05813690328693,0.0872664626099692);
#107=FACE_BOUND('',#474,.T.);
#125=TOROIDAL_SURFACE('',#3562,2.37846096908266,0.2);
#129=PLANE('',#3524);
#130=PLANE('',#3526);
#131=PLANE('',#3529);
#132=PLANE('',#3534);
#133=PLANE('',#3536);
#134=PLANE('',#3539);
#135=PLANE('',#3545);
#136=PLANE('',#3550);
#137=PLANE('',#3552);
#138=PLANE('',#3554);
#139=PLANE('',#3557);
#140=PLANE('',#3559);
#141=PLANE('',#3561);
#142=PLANE('',#3566);
#143=PLANE('',#3574);
#266=FACE_OUTER_BOUND('',#455,.T.);
#267=FACE_OUTER_BOUND('',#456,.T.);
#268=FACE_OUTER_BOUND('',#457,.T.);
#269=FACE_OUTER_BOUND('',#458,.T.);
#270=FACE_OUTER_BOUND('',#459,.T.);
#271=FACE_OUTER_BOUND('',#460,.T.);
#272=FACE_OUTER_BOUND('',#461,.T.);
#273=FACE_OUTER_BOUND('',#462,.T.);
#274=FACE_OUTER_BOUND('',#463,.T.);
#275=FACE_OUTER_BOUND('',#464,.T.);
#276=FACE_OUTER_BOUND('',#465,.T.);
#277=FACE_OUTER_BOUND('',#466,.T.);
#278=FACE_OUTER_BOUND('',#467,.T.);
#279=FACE_OUTER_BOUND('',#468,.T.);
#280=FACE_OUTER_BOUND('',#469,.T.);
#281=FACE_OUTER_BOUND('',#470,.T.);
#282=FACE_OUTER_BOUND('',#471,.T.);
#283=FACE_OUTER_BOUND('',#472,.T.);
#284=FACE_OUTER_BOUND('',#473,.T.);
#285=FACE_OUTER_BOUND('',#475,.T.);
#286=FACE_OUTER_BOUND('',#476,.T.);
#287=FACE_OUTER_BOUND('',#477,.T.);
#288=FACE_OUTER_BOUND('',#478,.T.);
#289=FACE_OUTER_BOUND('',#479,.T.);
#290=FACE_OUTER_BOUND('',#480,.T.);
#455=EDGE_LOOP('',(#2221,#2222,#2223,#2224,#2225,#2226));
#456=EDGE_LOOP('',(#2227,#2228,#2229));
#457=EDGE_LOOP('',(#2230,#2231,#2232,#2233,#2234,#2235));
#458=EDGE_LOOP('',(#2236,#2237,#2238));
#459=EDGE_LOOP('',(#2239,#2240,#2241,#2242,#2243,#2244));
#460=EDGE_LOOP('',(#2245,#2246,#2247));
#461=EDGE_LOOP('',(#2248,#2249,#2250,#2251,#2252,#2253));
#462=EDGE_LOOP('',(#2254,#2255,#2256));
#463=EDGE_LOOP('',(#2257,#2258,#2259,#2260,#2261,#2262));
#464=EDGE_LOOP('',(#2263,#2264,#2265));
#465=EDGE_LOOP('',(#2266,#2267,#2268,#2269,#2270,#2271));
#466=EDGE_LOOP('',(#2272,#2273,#2274));
#467=EDGE_LOOP('',(#2275,#2276,#2277));
#468=EDGE_LOOP('',(#2278,#2279,#2280,#2281,#2282,#2283,#2284));
#469=EDGE_LOOP('',(#2285,#2286,#2287));
#470=EDGE_LOOP('',(#2288,#2289,#2290,#2291,#2292,#2293));
#471=EDGE_LOOP('',(#2294,#2295,#2296,#2297,#2298,#2299,#2300,#2301));
#472=EDGE_LOOP('',(#2302,#2303,#2304,#2305));
#473=EDGE_LOOP('',(#2306));
#474=EDGE_LOOP('',(#2307));
#475=EDGE_LOOP('',(#2308,#2309,#2310,#2311));
#476=EDGE_LOOP('',(#2312,#2313,#2314,#2315));
#477=EDGE_LOOP('',(#2316,#2317,#2318,#2319));
#478=EDGE_LOOP('',(#2320));
#479=EDGE_LOOP('',(#2321,#2322,#2323,#2324,#2325,#2326,#2327,#2328,#2329,
#2330,#2331,#2332,#2333,#2334,#2335,#2336,#2337,#2338,#2339,#2340,#2341));
#480=EDGE_LOOP('',(#2342,#2343,#2344,#2345,#2346));
#662=CIRCLE('',#3522,0.946);
#663=CIRCLE('',#3525,12.8232171353527);
#664=CIRCLE('',#3527,12.1073709048319);
#665=CIRCLE('',#3530,12.8232171353527);
#666=CIRCLE('',#3532,0.946);
#667=CIRCLE('',#3535,12.8232171353527);
#668=CIRCLE('',#3537,12.1073709048319);
#669=CIRCLE('',#3540,12.8232171353527);
#670=CIRCLE('',#3543,0.946);
#671=CIRCLE('',#3546,12.8232171353527);
#672=CIRCLE('',#3548,0.946);
#673=CIRCLE('',#3551,12.8232171353527);
#674=CIRCLE('',#3553,12.8232171353527);
#675=CIRCLE('',#3555,12.1073709048319);
#676=CIRCLE('',#3556,12.1073709048319);
#677=CIRCLE('',#3558,12.8232171353527);
#678=CIRCLE('',#3560,12.1073709048319);
#679=CIRCLE('',#3563,2.37846096908266);
#680=CIRCLE('',#3564,0.2);
#681=CIRCLE('',#3565,2.17846096908266);
#682=CIRCLE('',#3567,5.15);
#683=CIRCLE('',#3569,2.17846096908266);
#684=CIRCLE('',#3571,2.4505);
#685=CIRCLE('',#3573,2.4505);
#686=CIRCLE('',#3576,12.8319377609308);
#687=CIRCLE('',#3577,4.96627380657387);
#688=CIRCLE('',#3578,4.96627380657387);
#795=ELLIPSE('',#3521,1.892,0.946);
#796=ELLIPSE('',#3523,1.892,0.946);
#797=ELLIPSE('',#3528,1.892,0.946);
#798=ELLIPSE('',#3533,1.892,0.946);
#799=ELLIPSE('',#3538,1.892,0.946);
#800=ELLIPSE('',#3542,1.892,0.946);
#801=ELLIPSE('',#3544,1.892,0.946);
#802=ELLIPSE('',#3549,1.892,0.946);
#827=LINE('',#4955,#1121);
#828=LINE('',#4962,#1122);
#829=LINE('',#4966,#1123);
#830=LINE('',#4971,#1124);
#831=LINE('',#4974,#1125);
#832=LINE('',#4978,#1126);
#833=LINE('',#5000,#1127);
#834=LINE('',#5004,#1128);
#835=LINE('',#5009,#1129);
#836=LINE('',#5012,#1130);
#837=LINE('',#5016,#1131);
#838=LINE('',#5036,#1132);
#839=LINE('',#5043,#1133);
#840=LINE('',#5047,#1134);
#841=LINE('',#5069,#1135);
#842=LINE('',#5073,#1136);
#843=LINE('',#5077,#1137);
#844=LINE('',#5081,#1138);
#845=LINE('',#5086,#1139);
#846=LINE('',#5089,#1140);
#847=LINE('',#5103,#1141);
#848=LINE('',#5107,#1142);
#849=LINE('',#5111,#1143);
#850=LINE('',#5120,#1144);
#1121=VECTOR('',#3898,10.);
#1122=VECTOR('',#3905,10.);
#1123=VECTOR('',#3910,10.);
#1124=VECTOR('',#3915,10.);
#1125=VECTOR('',#3918,10.);
#1126=VECTOR('',#3923,10.);
#1127=VECTOR('',#3930,10.);
#1128=VECTOR('',#3935,10.);
#1129=VECTOR('',#3940,10.);
#1130=VECTOR('',#3943,10.);
#1131=VECTOR('',#3948,10.);
#1132=VECTOR('',#3951,10.);
#1133=VECTOR('',#3958,10.);
#1134=VECTOR('',#3963,10.);
#1135=VECTOR('',#3970,10.);
#1136=VECTOR('',#3975,10.);
#1137=VECTOR('',#3980,10.);
#1138=VECTOR('',#3985,10.);
#1139=VECTOR('',#3992,10.);
#1140=VECTOR('',#3997,10.);
#1141=VECTOR('',#4016,2.17846096908266);
#1142=VECTOR('',#4021,2.33923048454133);
#1143=VECTOR('',#4026,2.5);
#1144=VECTOR('',#4039,5.05813690328693);
#1415=B_SPLINE_CURVE_WITH_KNOTS('',3,(#4939,#4940,#4941,#4942,#4943,#4944,
#4945,#4946,#4947,#4948,#4949,#4950,#4951,#4952,#4953),.UNSPECIFIED.,.F.,
 .F.,(4,2,2,3,2,2,4),(-0.0714521071173775,-0.0712222400952786,-0.0356111200476392,
0.,0.0356111200476392,0.0712222400952784,0.0714521071173274),
 .UNSPECIFIED.);
#1416=B_SPLINE_CURVE_WITH_KNOTS('',3,(#4981,#4982,#4983,#4984,#4985,#4986,
#4987,#4988,#4989,#4990,#4991,#4992,#4993,#4994,#4995),.UNSPECIFIED.,.F.,
 .F.,(4,2,2,3,2,2,4),(-0.071452107117379,-0.0712222400952786,-0.0356111200476392,
0.,0.0356111200476392,0.0712222400952784,0.071452107117329),
 .UNSPECIFIED.);
#1417=B_SPLINE_CURVE_WITH_KNOTS('',3,(#5020,#5021,#5022,#5023,#5024,#5025,
#5026,#5027,#5028,#5029,#5030,#5031,#5032,#5033,#5034),.UNSPECIFIED.,.F.,
 .F.,(4,2,2,3,2,2,4),(-0.0714521071173781,-0.0712222400952784,-0.0356111200476392,
0.,0.0356111200476392,0.0712222400952785,0.0714521071173282),
 .UNSPECIFIED.);
#1418=B_SPLINE_CURVE_WITH_KNOTS('',3,(#5050,#5051,#5052,#5053,#5054,#5055,
#5056,#5057,#5058,#5059,#5060,#5061,#5062,#5063,#5064),.UNSPECIFIED.,.F.,
 .F.,(4,2,2,3,2,2,4),(-0.0714521071173768,-0.0712222400952786,-0.0356111200476392,
0.,0.0356111200476392,0.0712222400952785,0.0714521071173268),
 .UNSPECIFIED.);
#1432=VERTEX_POINT('',#4937);
#1433=VERTEX_POINT('',#4938);
#1434=VERTEX_POINT('',#4954);
#1435=VERTEX_POINT('',#4956);
#1436=VERTEX_POINT('',#4958);
#1437=VERTEX_POINT('',#4960);
#1438=VERTEX_POINT('',#4964);
#1439=VERTEX_POINT('',#4968);
#1440=VERTEX_POINT('',#4970);
#1441=VERTEX_POINT('',#4972);
#1442=VERTEX_POINT('',#4976);
#1443=VERTEX_POINT('',#4980);
#1444=VERTEX_POINT('',#4996);
#1445=VERTEX_POINT('',#4998);
#1446=VERTEX_POINT('',#5002);
#1447=VERTEX_POINT('',#5006);
#1448=VERTEX_POINT('',#5008);
#1449=VERTEX_POINT('',#5010);
#1450=VERTEX_POINT('',#5014);
#1451=VERTEX_POINT('',#5018);
#1452=VERTEX_POINT('',#5019);
#1453=VERTEX_POINT('',#5035);
#1454=VERTEX_POINT('',#5037);
#1455=VERTEX_POINT('',#5039);
#1456=VERTEX_POINT('',#5041);
#1457=VERTEX_POINT('',#5045);
#1458=VERTEX_POINT('',#5049);
#1459=VERTEX_POINT('',#5065);
#1460=VERTEX_POINT('',#5067);
#1461=VERTEX_POINT('',#5071);
#1462=VERTEX_POINT('',#5075);
#1463=VERTEX_POINT('',#5079);
#1464=VERTEX_POINT('',#5084);
#1465=VERTEX_POINT('',#5092);
#1466=VERTEX_POINT('',#5094);
#1467=VERTEX_POINT('',#5098);
#1468=VERTEX_POINT('',#5101);
#1469=VERTEX_POINT('',#5105);
#1470=VERTEX_POINT('',#5109);
#1471=VERTEX_POINT('',#5114);
#1472=VERTEX_POINT('',#5116);
#1745=EDGE_CURVE('',#1432,#1433,#1415,.T.);
#1746=EDGE_CURVE('',#1434,#1432,#827,.T.);
#1747=EDGE_CURVE('',#1434,#1435,#795,.F.);
#1748=EDGE_CURVE('',#1435,#1436,#662,.F.);
#1749=EDGE_CURVE('',#1437,#1436,#796,.T.);
#1750=EDGE_CURVE('',#1433,#1437,#828,.T.);
#1751=EDGE_CURVE('',#1433,#1438,#663,.T.);
#1752=EDGE_CURVE('',#1438,#1437,#829,.F.);
#1753=EDGE_CURVE('',#1438,#1439,#664,.T.);
#1754=EDGE_CURVE('',#1436,#1440,#830,.F.);
#1755=EDGE_CURVE('',#1441,#1440,#797,.F.);
#1756=EDGE_CURVE('',#1439,#1441,#831,.T.);
#1757=EDGE_CURVE('',#1439,#1442,#665,.T.);
#1758=EDGE_CURVE('',#1441,#1442,#832,.T.);
#1759=EDGE_CURVE('',#1442,#1443,#1416,.T.);
#1760=EDGE_CURVE('',#1440,#1444,#666,.F.);
#1761=EDGE_CURVE('',#1445,#1444,#798,.T.);
#1762=EDGE_CURVE('',#1443,#1445,#833,.T.);
#1763=EDGE_CURVE('',#1443,#1446,#667,.T.);
#1764=EDGE_CURVE('',#1446,#1445,#834,.F.);
#1765=EDGE_CURVE('',#1446,#1447,#668,.T.);
#1766=EDGE_CURVE('',#1444,#1448,#835,.F.);
#1767=EDGE_CURVE('',#1449,#1448,#799,.F.);
#1768=EDGE_CURVE('',#1447,#1449,#836,.T.);
#1769=EDGE_CURVE('',#1447,#1450,#669,.T.);
#1770=EDGE_CURVE('',#1449,#1450,#837,.T.);
#1771=EDGE_CURVE('',#1451,#1452,#1417,.T.);
#1772=EDGE_CURVE('',#1453,#1451,#838,.T.);
#1773=EDGE_CURVE('',#1453,#1454,#800,.F.);
#1774=EDGE_CURVE('',#1454,#1455,#670,.F.);
#1775=EDGE_CURVE('',#1456,#1455,#801,.T.);
#1776=EDGE_CURVE('',#1452,#1456,#839,.T.);
#1777=EDGE_CURVE('',#1452,#1457,#671,.T.);
#1778=EDGE_CURVE('',#1457,#1456,#840,.F.);
#1779=EDGE_CURVE('',#1450,#1458,#1418,.T.);
#1780=EDGE_CURVE('',#1448,#1459,#672,.F.);
#1781=EDGE_CURVE('',#1460,#1459,#802,.T.);
#1782=EDGE_CURVE('',#1458,#1460,#841,.T.);
#1783=EDGE_CURVE('',#1458,#1461,#673,.T.);
#1784=EDGE_CURVE('',#1461,#1460,#842,.F.);
#1785=EDGE_CURVE('',#1462,#1432,#674,.T.);
#1786=EDGE_CURVE('',#1462,#1434,#843,.T.);
#1787=EDGE_CURVE('',#1457,#1463,#675,.T.);
#1788=EDGE_CURVE('',#1455,#1435,#844,.F.);
#1789=EDGE_CURVE('',#1463,#1462,#676,.T.);
#1790=EDGE_CURVE('',#1464,#1451,#677,.T.);
#1791=EDGE_CURVE('',#1464,#1453,#845,.T.);
#1792=EDGE_CURVE('',#1461,#1464,#678,.T.);
#1793=EDGE_CURVE('',#1459,#1454,#846,.F.);
#1794=EDGE_CURVE('',#1465,#1465,#679,.T.);
#1795=EDGE_CURVE('',#1465,#1466,#680,.T.);
#1796=EDGE_CURVE('',#1466,#1466,#681,.T.);
#1797=EDGE_CURVE('',#1467,#1467,#682,.T.);
#1798=EDGE_CURVE('',#1468,#1468,#683,.T.);
#1799=EDGE_CURVE('',#1468,#1466,#847,.T.);
#1800=EDGE_CURVE('',#1469,#1469,#684,.T.);
#1801=EDGE_CURVE('',#1469,#1468,#848,.T.);
#1802=EDGE_CURVE('',#1470,#1470,#685,.F.);
#1803=EDGE_CURVE('',#1470,#1469,#849,.T.);
#1804=EDGE_CURVE('',#1463,#1471,#686,.T.);
#1805=EDGE_CURVE('',#1472,#1471,#687,.T.);
#1806=EDGE_CURVE('',#1471,#1472,#688,.T.);
#1807=EDGE_CURVE('',#1467,#1472,#850,.T.);
#2221=ORIENTED_EDGE('',*,*,#1745,.F.);
#2222=ORIENTED_EDGE('',*,*,#1746,.F.);
#2223=ORIENTED_EDGE('',*,*,#1747,.T.);
#2224=ORIENTED_EDGE('',*,*,#1748,.T.);
#2225=ORIENTED_EDGE('',*,*,#1749,.F.);
#2226=ORIENTED_EDGE('',*,*,#1750,.F.);
#2227=ORIENTED_EDGE('',*,*,#1751,.F.);
#2228=ORIENTED_EDGE('',*,*,#1750,.T.);
#2229=ORIENTED_EDGE('',*,*,#1752,.F.);
#2230=ORIENTED_EDGE('',*,*,#1753,.F.);
#2231=ORIENTED_EDGE('',*,*,#1752,.T.);
#2232=ORIENTED_EDGE('',*,*,#1749,.T.);
#2233=ORIENTED_EDGE('',*,*,#1754,.T.);
#2234=ORIENTED_EDGE('',*,*,#1755,.F.);
#2235=ORIENTED_EDGE('',*,*,#1756,.F.);
#2236=ORIENTED_EDGE('',*,*,#1757,.F.);
#2237=ORIENTED_EDGE('',*,*,#1756,.T.);
#2238=ORIENTED_EDGE('',*,*,#1758,.T.);
#2239=ORIENTED_EDGE('',*,*,#1759,.F.);
#2240=ORIENTED_EDGE('',*,*,#1758,.F.);
#2241=ORIENTED_EDGE('',*,*,#1755,.T.);
#2242=ORIENTED_EDGE('',*,*,#1760,.T.);
#2243=ORIENTED_EDGE('',*,*,#1761,.F.);
#2244=ORIENTED_EDGE('',*,*,#1762,.F.);
#2245=ORIENTED_EDGE('',*,*,#1763,.F.);
#2246=ORIENTED_EDGE('',*,*,#1762,.T.);
#2247=ORIENTED_EDGE('',*,*,#1764,.F.);
#2248=ORIENTED_EDGE('',*,*,#1765,.F.);
#2249=ORIENTED_EDGE('',*,*,#1764,.T.);
#2250=ORIENTED_EDGE('',*,*,#1761,.T.);
#2251=ORIENTED_EDGE('',*,*,#1766,.T.);
#2252=ORIENTED_EDGE('',*,*,#1767,.F.);
#2253=ORIENTED_EDGE('',*,*,#1768,.F.);
#2254=ORIENTED_EDGE('',*,*,#1769,.F.);
#2255=ORIENTED_EDGE('',*,*,#1768,.T.);
#2256=ORIENTED_EDGE('',*,*,#1770,.T.);
#2257=ORIENTED_EDGE('',*,*,#1771,.F.);
#2258=ORIENTED_EDGE('',*,*,#1772,.F.);
#2259=ORIENTED_EDGE('',*,*,#1773,.T.);
#2260=ORIENTED_EDGE('',*,*,#1774,.T.);
#2261=ORIENTED_EDGE('',*,*,#1775,.F.);
#2262=ORIENTED_EDGE('',*,*,#1776,.F.);
#2263=ORIENTED_EDGE('',*,*,#1777,.F.);
#2264=ORIENTED_EDGE('',*,*,#1776,.T.);
#2265=ORIENTED_EDGE('',*,*,#1778,.F.);
#2266=ORIENTED_EDGE('',*,*,#1779,.F.);
#2267=ORIENTED_EDGE('',*,*,#1770,.F.);
#2268=ORIENTED_EDGE('',*,*,#1767,.T.);
#2269=ORIENTED_EDGE('',*,*,#1780,.T.);
#2270=ORIENTED_EDGE('',*,*,#1781,.F.);
#2271=ORIENTED_EDGE('',*,*,#1782,.F.);
#2272=ORIENTED_EDGE('',*,*,#1783,.F.);
#2273=ORIENTED_EDGE('',*,*,#1782,.T.);
#2274=ORIENTED_EDGE('',*,*,#1784,.F.);
#2275=ORIENTED_EDGE('',*,*,#1785,.F.);
#2276=ORIENTED_EDGE('',*,*,#1786,.T.);
#2277=ORIENTED_EDGE('',*,*,#1746,.T.);
#2278=ORIENTED_EDGE('',*,*,#1787,.F.);
#2279=ORIENTED_EDGE('',*,*,#1778,.T.);
#2280=ORIENTED_EDGE('',*,*,#1775,.T.);
#2281=ORIENTED_EDGE('',*,*,#1788,.T.);
#2282=ORIENTED_EDGE('',*,*,#1747,.F.);
#2283=ORIENTED_EDGE('',*,*,#1786,.F.);
#2284=ORIENTED_EDGE('',*,*,#1789,.F.);
#2285=ORIENTED_EDGE('',*,*,#1790,.F.);
#2286=ORIENTED_EDGE('',*,*,#1791,.T.);
#2287=ORIENTED_EDGE('',*,*,#1772,.T.);
#2288=ORIENTED_EDGE('',*,*,#1792,.F.);
#2289=ORIENTED_EDGE('',*,*,#1784,.T.);
#2290=ORIENTED_EDGE('',*,*,#1781,.T.);
#2291=ORIENTED_EDGE('',*,*,#1793,.T.);
#2292=ORIENTED_EDGE('',*,*,#1773,.F.);
#2293=ORIENTED_EDGE('',*,*,#1791,.F.);
#2294=ORIENTED_EDGE('',*,*,#1754,.F.);
#2295=ORIENTED_EDGE('',*,*,#1748,.F.);
#2296=ORIENTED_EDGE('',*,*,#1788,.F.);
#2297=ORIENTED_EDGE('',*,*,#1774,.F.);
#2298=ORIENTED_EDGE('',*,*,#1793,.F.);
#2299=ORIENTED_EDGE('',*,*,#1780,.F.);
#2300=ORIENTED_EDGE('',*,*,#1766,.F.);
#2301=ORIENTED_EDGE('',*,*,#1760,.F.);
#2302=ORIENTED_EDGE('',*,*,#1794,.T.);
#2303=ORIENTED_EDGE('',*,*,#1795,.T.);
#2304=ORIENTED_EDGE('',*,*,#1796,.T.);
#2305=ORIENTED_EDGE('',*,*,#1795,.F.);
#2306=ORIENTED_EDGE('',*,*,#1797,.T.);
#2307=ORIENTED_EDGE('',*,*,#1794,.F.);
#2308=ORIENTED_EDGE('',*,*,#1798,.F.);
#2309=ORIENTED_EDGE('',*,*,#1799,.T.);
#2310=ORIENTED_EDGE('',*,*,#1796,.F.);
#2311=ORIENTED_EDGE('',*,*,#1799,.F.);
#2312=ORIENTED_EDGE('',*,*,#1800,.F.);
#2313=ORIENTED_EDGE('',*,*,#1801,.T.);
#2314=ORIENTED_EDGE('',*,*,#1798,.T.);
#2315=ORIENTED_EDGE('',*,*,#1801,.F.);
#2316=ORIENTED_EDGE('',*,*,#1802,.F.);
#2317=ORIENTED_EDGE('',*,*,#1803,.T.);
#2318=ORIENTED_EDGE('',*,*,#1800,.T.);
#2319=ORIENTED_EDGE('',*,*,#1803,.F.);
#2320=ORIENTED_EDGE('',*,*,#1802,.T.);
#2321=ORIENTED_EDGE('',*,*,#1779,.T.);
#2322=ORIENTED_EDGE('',*,*,#1783,.T.);
#2323=ORIENTED_EDGE('',*,*,#1792,.T.);
#2324=ORIENTED_EDGE('',*,*,#1790,.T.);
#2325=ORIENTED_EDGE('',*,*,#1771,.T.);
#2326=ORIENTED_EDGE('',*,*,#1777,.T.);
#2327=ORIENTED_EDGE('',*,*,#1787,.T.);
#2328=ORIENTED_EDGE('',*,*,#1804,.T.);
#2329=ORIENTED_EDGE('',*,*,#1805,.F.);
#2330=ORIENTED_EDGE('',*,*,#1806,.F.);
#2331=ORIENTED_EDGE('',*,*,#1804,.F.);
#2332=ORIENTED_EDGE('',*,*,#1789,.T.);
#2333=ORIENTED_EDGE('',*,*,#1785,.T.);
#2334=ORIENTED_EDGE('',*,*,#1745,.T.);
#2335=ORIENTED_EDGE('',*,*,#1751,.T.);
#2336=ORIENTED_EDGE('',*,*,#1753,.T.);
#2337=ORIENTED_EDGE('',*,*,#1757,.T.);
#2338=ORIENTED_EDGE('',*,*,#1759,.T.);
#2339=ORIENTED_EDGE('',*,*,#1763,.T.);
#2340=ORIENTED_EDGE('',*,*,#1765,.T.);
#2341=ORIENTED_EDGE('',*,*,#1769,.T.);
#2342=ORIENTED_EDGE('',*,*,#1797,.F.);
#2343=ORIENTED_EDGE('',*,*,#1807,.T.);
#2344=ORIENTED_EDGE('',*,*,#1805,.T.);
#2345=ORIENTED_EDGE('',*,*,#1806,.T.);
#2346=ORIENTED_EDGE('',*,*,#1807,.F.);
#3173=CYLINDRICAL_SURFACE('',#3520,0.946);
#3174=CYLINDRICAL_SURFACE('',#3531,0.946);
#3175=CYLINDRICAL_SURFACE('',#3541,0.946);
#3176=CYLINDRICAL_SURFACE('',#3547,0.946);
#3177=CYLINDRICAL_SURFACE('',#3568,2.17846096908266);
#3178=CYLINDRICAL_SURFACE('',#3572,2.4505);
#3208=ADVANCED_FACE('',(#266),#3173,.T.);
#3209=ADVANCED_FACE('',(#267),#129,.F.);
#3210=ADVANCED_FACE('',(#268),#130,.F.);
#3211=ADVANCED_FACE('',(#269),#131,.F.);
#3212=ADVANCED_FACE('',(#270),#3174,.T.);
#3213=ADVANCED_FACE('',(#271),#132,.F.);
#3214=ADVANCED_FACE('',(#272),#133,.F.);
#3215=ADVANCED_FACE('',(#273),#134,.F.);
#3216=ADVANCED_FACE('',(#274),#3175,.T.);
#3217=ADVANCED_FACE('',(#275),#135,.F.);
#3218=ADVANCED_FACE('',(#276),#3176,.T.);
#3219=ADVANCED_FACE('',(#277),#136,.F.);
#3220=ADVANCED_FACE('',(#278),#137,.F.);
#3221=ADVANCED_FACE('',(#279),#138,.F.);
#3222=ADVANCED_FACE('',(#280),#139,.F.);
#3223=ADVANCED_FACE('',(#281),#140,.F.);
#3224=ADVANCED_FACE('',(#282),#141,.F.);
#3225=ADVANCED_FACE('',(#283),#125,.F.);
#3226=ADVANCED_FACE('',(#284,#107),#142,.T.);
#3227=ADVANCED_FACE('',(#285),#3177,.T.);
#3228=ADVANCED_FACE('',(#286),#99,.T.);
#3229=ADVANCED_FACE('',(#287),#3178,.T.);
#3230=ADVANCED_FACE('',(#288),#143,.T.);
#3231=ADVANCED_FACE('',(#289),#95,.T.);
#3232=ADVANCED_FACE('',(#290),#100,.T.);
#3397=CLOSED_SHELL('',(#3208,#3209,#3210,#3211,#3212,#3213,#3214,#3215,
#3216,#3217,#3218,#3219,#3220,#3221,#3222,#3223,#3224,#3225,#3226,#3227,
#3228,#3229,#3230,#3231,#3232));
#3519=AXIS2_PLACEMENT_3D('',#4935,#3894,#3895);
#3520=AXIS2_PLACEMENT_3D('',#4936,#3896,#3897);
#3521=AXIS2_PLACEMENT_3D('',#4957,#3899,#3900);
#3522=AXIS2_PLACEMENT_3D('',#4959,#3901,#3902);
#3523=AXIS2_PLACEMENT_3D('',#4961,#3903,#3904);
#3524=AXIS2_PLACEMENT_3D('',#4963,#3906,#3907);
#3525=AXIS2_PLACEMENT_3D('',#4965,#3908,#3909);
#3526=AXIS2_PLACEMENT_3D('',#4967,#3911,#3912);
#3527=AXIS2_PLACEMENT_3D('',#4969,#3913,#3914);
#3528=AXIS2_PLACEMENT_3D('',#4973,#3916,#3917);
#3529=AXIS2_PLACEMENT_3D('',#4975,#3919,#3920);
#3530=AXIS2_PLACEMENT_3D('',#4977,#3921,#3922);
#3531=AXIS2_PLACEMENT_3D('',#4979,#3924,#3925);
#3532=AXIS2_PLACEMENT_3D('',#4997,#3926,#3927);
#3533=AXIS2_PLACEMENT_3D('',#4999,#3928,#3929);
#3534=AXIS2_PLACEMENT_3D('',#5001,#3931,#3932);
#3535=AXIS2_PLACEMENT_3D('',#5003,#3933,#3934);
#3536=AXIS2_PLACEMENT_3D('',#5005,#3936,#3937);
#3537=AXIS2_PLACEMENT_3D('',#5007,#3938,#3939);
#3538=AXIS2_PLACEMENT_3D('',#5011,#3941,#3942);
#3539=AXIS2_PLACEMENT_3D('',#5013,#3944,#3945);
#3540=AXIS2_PLACEMENT_3D('',#5015,#3946,#3947);
#3541=AXIS2_PLACEMENT_3D('',#5017,#3949,#3950);
#3542=AXIS2_PLACEMENT_3D('',#5038,#3952,#3953);
#3543=AXIS2_PLACEMENT_3D('',#5040,#3954,#3955);
#3544=AXIS2_PLACEMENT_3D('',#5042,#3956,#3957);
#3545=AXIS2_PLACEMENT_3D('',#5044,#3959,#3960);
#3546=AXIS2_PLACEMENT_3D('',#5046,#3961,#3962);
#3547=AXIS2_PLACEMENT_3D('',#5048,#3964,#3965);
#3548=AXIS2_PLACEMENT_3D('',#5066,#3966,#3967);
#3549=AXIS2_PLACEMENT_3D('',#5068,#3968,#3969);
#3550=AXIS2_PLACEMENT_3D('',#5070,#3971,#3972);
#3551=AXIS2_PLACEMENT_3D('',#5072,#3973,#3974);
#3552=AXIS2_PLACEMENT_3D('',#5074,#3976,#3977);
#3553=AXIS2_PLACEMENT_3D('',#5076,#3978,#3979);
#3554=AXIS2_PLACEMENT_3D('',#5078,#3981,#3982);
#3555=AXIS2_PLACEMENT_3D('',#5080,#3983,#3984);
#3556=AXIS2_PLACEMENT_3D('',#5082,#3986,#3987);
#3557=AXIS2_PLACEMENT_3D('',#5083,#3988,#3989);
#3558=AXIS2_PLACEMENT_3D('',#5085,#3990,#3991);
#3559=AXIS2_PLACEMENT_3D('',#5087,#3993,#3994);
#3560=AXIS2_PLACEMENT_3D('',#5088,#3995,#3996);
#3561=AXIS2_PLACEMENT_3D('',#5090,#3998,#3999);
#3562=AXIS2_PLACEMENT_3D('',#5091,#4000,#4001);
#3563=AXIS2_PLACEMENT_3D('',#5093,#4002,#4003);
#3564=AXIS2_PLACEMENT_3D('',#5095,#4004,#4005);
#3565=AXIS2_PLACEMENT_3D('',#5096,#4006,#4007);
#3566=AXIS2_PLACEMENT_3D('',#5097,#4008,#4009);
#3567=AXIS2_PLACEMENT_3D('',#5099,#4010,#4011);
#3568=AXIS2_PLACEMENT_3D('',#5100,#4012,#4013);
#3569=AXIS2_PLACEMENT_3D('',#5102,#4014,#4015);
#3570=AXIS2_PLACEMENT_3D('',#5104,#4017,#4018);
#3571=AXIS2_PLACEMENT_3D('',#5106,#4019,#4020);
#3572=AXIS2_PLACEMENT_3D('',#5108,#4022,#4023);
#3573=AXIS2_PLACEMENT_3D('',#5110,#4024,#4025);
#3574=AXIS2_PLACEMENT_3D('',#5112,#4027,#4028);
#3575=AXIS2_PLACEMENT_3D('',#5113,#4029,#4030);
#3576=AXIS2_PLACEMENT_3D('',#5115,#4031,#4032);
#3577=AXIS2_PLACEMENT_3D('',#5117,#4033,#4034);
#3578=AXIS2_PLACEMENT_3D('',#5118,#4035,#4036);
#3579=AXIS2_PLACEMENT_3D('',#5119,#4037,#4038);
#3894=DIRECTION('axis',(0.,0.,1.));
#3895=DIRECTION('refdir',(1.,0.,0.));
#3896=DIRECTION('center_axis',(0.,0.,-1.));
#3897=DIRECTION('ref_axis',(0.707106781186563,-0.707106781186532,0.));
#3898=DIRECTION('',(0.,0.,1.));
#3899=DIRECTION('center_axis',(-0.866025403784439,0.,-0.5));
#3900=DIRECTION('ref_axis',(0.5,0.,-0.866025403784439));
#3901=DIRECTION('center_axis',(0.,0.,-1.));
#3902=DIRECTION('ref_axis',(0.707106781186563,-0.707106781186532,0.));
#3903=DIRECTION('center_axis',(-2.54091264057109E-15,0.866025403784439,
-0.5));
#3904=DIRECTION('ref_axis',(1.43032168209504E-15,-0.5,-0.866025403784439));
#3905=DIRECTION('',(0.,0.,-1.));
#3906=DIRECTION('center_axis',(-1.,-4.30300426108057E-14,0.));
#3907=DIRECTION('ref_axis',(-4.30300426108057E-14,1.,0.));
#3908=DIRECTION('center_axis',(-1.,-4.30300426108057E-14,0.));
#3909=DIRECTION('ref_axis',(0.,0.,-1.));
#3910=DIRECTION('',(-2.15150213054029E-14,0.5,0.866025403784439));
#3911=DIRECTION('center_axis',(-2.54091264057109E-15,0.866025403784439,
-0.5));
#3912=DIRECTION('ref_axis',(1.,2.93399319404209E-15,0.));
#3913=DIRECTION('center_axis',(-2.54091264057109E-15,0.866025403784439,
-0.5));
#3914=DIRECTION('ref_axis',(0.,-0.5,-0.866025403784439));
#3915=DIRECTION('',(-1.,-2.93399319404209E-15,0.));
#3916=DIRECTION('center_axis',(-2.54091264057109E-15,0.866025403784439,
-0.5));
#3917=DIRECTION('ref_axis',(1.46699659702056E-15,-0.5,-0.866025403784439));
#3918=DIRECTION('',(-1.73044443434865E-14,-0.5,-0.866025403784439));
#3919=DIRECTION('center_axis',(1.,-3.4608888686973E-14,0.));
#3920=DIRECTION('ref_axis',(-3.4608888686973E-14,-1.,0.));
#3921=DIRECTION('center_axis',(1.,-3.4608888686973E-14,0.));
#3922=DIRECTION('ref_axis',(0.,0.,1.));
#3923=DIRECTION('',(0.,0.,1.));
#3924=DIRECTION('center_axis',(0.,0.,-1.));
#3925=DIRECTION('ref_axis',(-0.707106781186546,-0.707106781186549,0.));
#3926=DIRECTION('center_axis',(0.,0.,-1.));
#3927=DIRECTION('ref_axis',(-0.707106781186546,-0.707106781186549,0.));
#3928=DIRECTION('center_axis',(0.866025403784439,0.,-0.5));
#3929=DIRECTION('ref_axis',(-0.5,-3.66749149255139E-17,-0.866025403784439));
#3930=DIRECTION('',(0.,0.,-1.));
#3931=DIRECTION('center_axis',(-4.04626176340286E-14,1.,0.));
#3932=DIRECTION('ref_axis',(1.,4.04626176340286E-14,0.));
#3933=DIRECTION('center_axis',(-4.04626176340286E-14,1.,0.));
#3934=DIRECTION('ref_axis',(0.,0.,-1.));
#3935=DIRECTION('',(0.5,2.02313088170143E-14,0.866025403784439));
#3936=DIRECTION('center_axis',(0.866025403784439,0.,-0.5));
#3937=DIRECTION('ref_axis',(0.,-1.,0.));
#3938=DIRECTION('center_axis',(0.866025403784439,0.,-0.5));
#3939=DIRECTION('ref_axis',(0.5,0.,0.866025403784439));
#3940=DIRECTION('',(0.,1.,0.));
#3941=DIRECTION('center_axis',(0.866025403784439,0.,-0.5));
#3942=DIRECTION('ref_axis',(-0.5,3.66749149255139E-17,-0.866025403784439));
#3943=DIRECTION('',(-0.5,2.39626331165986E-16,-0.866025403784439));
#3944=DIRECTION('center_axis',(-4.79252662331972E-16,-1.,0.));
#3945=DIRECTION('ref_axis',(-1.,4.79252662331972E-16,0.));
#3946=DIRECTION('center_axis',(-4.79252662331972E-16,-1.,0.));
#3947=DIRECTION('ref_axis',(0.,0.,1.));
#3948=DIRECTION('',(0.,0.,1.));
#3949=DIRECTION('center_axis',(0.,0.,-1.));
#3950=DIRECTION('ref_axis',(0.70710678118653,0.707106781186565,0.));
#3951=DIRECTION('',(0.,0.,1.));
#3952=DIRECTION('center_axis',(-1.27045632028555E-15,-0.866025403784439,
-0.5));
#3953=DIRECTION('ref_axis',(6.96823383584764E-16,0.5,-0.866025403784439));
#3954=DIRECTION('center_axis',(0.,0.,-1.));
#3955=DIRECTION('ref_axis',(0.70710678118653,0.707106781186565,0.));
#3956=DIRECTION('center_axis',(-0.866025403784439,0.,-0.5));
#3957=DIRECTION('ref_axis',(0.5,3.66749149255139E-17,-0.866025403784439));
#3958=DIRECTION('',(0.,0.,-1.));
#3959=DIRECTION('center_axis',(5.35736011821097E-14,-1.,0.));
#3960=DIRECTION('ref_axis',(-1.,-5.35736011821097E-14,0.));
#3961=DIRECTION('center_axis',(5.35736011821097E-14,-1.,0.));
#3962=DIRECTION('ref_axis',(0.,0.,1.));
#3963=DIRECTION('',(-0.5,-2.67868005910549E-14,0.866025403784439));
#3964=DIRECTION('center_axis',(0.,0.,-1.));
#3965=DIRECTION('ref_axis',(-0.707106781186557,0.707106781186538,0.));
#3966=DIRECTION('center_axis',(0.,0.,-1.));
#3967=DIRECTION('ref_axis',(-0.707106781186557,0.707106781186538,0.));
#3968=DIRECTION('center_axis',(-1.27045632028555E-15,-0.866025403784439,
-0.5));
#3969=DIRECTION('ref_axis',(7.33498298510278E-16,0.5,-0.866025403784439));
#3970=DIRECTION('',(0.,0.,-1.));
#3971=DIRECTION('center_axis',(1.,2.81047454124667E-14,0.));
#3972=DIRECTION('ref_axis',(2.81047454124667E-14,-1.,0.));
#3973=DIRECTION('center_axis',(1.,2.81047454124667E-14,0.));
#3974=DIRECTION('ref_axis',(0.,0.,1.));
#3975=DIRECTION('',(1.40523727062334E-14,-0.5,0.866025403784439));
#3976=DIRECTION('center_axis',(0.,1.,0.));
#3977=DIRECTION('ref_axis',(1.,0.,0.));
#3978=DIRECTION('center_axis',(0.,1.,0.));
#3979=DIRECTION('ref_axis',(0.,0.,-1.));
#3980=DIRECTION('',(0.5,0.,-0.866025403784439));
#3981=DIRECTION('center_axis',(-0.866025403784439,0.,-0.5));
#3982=DIRECTION('ref_axis',(0.,1.,0.));
#3983=DIRECTION('center_axis',(-0.866025403784439,0.,-0.5));
#3984=DIRECTION('ref_axis',(0.5,0.,-0.866025403784439));
#3985=DIRECTION('',(0.,-1.,0.));
#3986=DIRECTION('center_axis',(-0.866025403784439,0.,-0.5));
#3987=DIRECTION('ref_axis',(0.5,0.,-0.866025403784439));
#3988=DIRECTION('center_axis',(-1.,3.8682536316795E-15,0.));
#3989=DIRECTION('ref_axis',(3.8682536316795E-15,1.,0.));
#3990=DIRECTION('center_axis',(-1.,3.8682536316795E-15,0.));
#3991=DIRECTION('ref_axis',(0.,0.,-1.));
#3992=DIRECTION('',(1.93412681583975E-15,0.5,-0.866025403784439));
#3993=DIRECTION('center_axis',(-1.27045632028555E-15,-0.866025403784439,
-0.5));
#3994=DIRECTION('ref_axis',(-1.,1.46699659702105E-15,0.));
#3995=DIRECTION('center_axis',(-1.27045632028555E-15,-0.866025403784439,
-0.5));
#3996=DIRECTION('ref_axis',(0.,-0.5,0.866025403784439));
#3997=DIRECTION('',(1.,-1.46699659702105E-15,0.));
#3998=DIRECTION('center_axis',(0.,0.,-1.));
#3999=DIRECTION('ref_axis',(-1.,0.,0.));
#4000=DIRECTION('center_axis',(0.,0.,-1.));
#4001=DIRECTION('ref_axis',(-1.,0.,0.));
#4002=DIRECTION('center_axis',(0.,0.,-1.));
#4003=DIRECTION('ref_axis',(1.,0.,0.));
#4004=DIRECTION('center_axis',(-1.22464679914735E-16,-1.,0.));
#4005=DIRECTION('ref_axis',(1.,-1.22464679914735E-16,0.));
#4006=DIRECTION('center_axis',(0.,0.,1.));
#4007=DIRECTION('ref_axis',(1.,0.,0.));
#4008=DIRECTION('center_axis',(0.,0.,-1.));
#4009=DIRECTION('ref_axis',(-1.,0.,0.));
#4010=DIRECTION('center_axis',(0.,0.,-1.));
#4011=DIRECTION('ref_axis',(1.,0.,0.));
#4012=DIRECTION('center_axis',(0.,0.,-1.));
#4013=DIRECTION('ref_axis',(-1.,0.,0.));
#4014=DIRECTION('center_axis',(0.,0.,-1.));
#4015=DIRECTION('ref_axis',(1.,0.,0.));
#4016=DIRECTION('',(0.,0.,1.));
#4017=DIRECTION('center_axis',(0.,0.,-1.));
#4018=DIRECTION('ref_axis',(-1.,0.,0.));
#4019=DIRECTION('center_axis',(0.,0.,-1.));
#4020=DIRECTION('ref_axis',(-1.,0.,0.));
#4021=DIRECTION('',(-0.258819045102519,3.16961915143174E-17,0.965925826289069));
#4022=DIRECTION('center_axis',(0.,0.,-1.));
#4023=DIRECTION('ref_axis',(-1.,0.,0.));
#4024=DIRECTION('center_axis',(0.,0.,1.));
#4025=DIRECTION('ref_axis',(-1.,0.,0.));
#4026=DIRECTION('',(0.,0.,1.));
#4027=DIRECTION('center_axis',(0.,0.,-1.));
#4028=DIRECTION('ref_axis',(-1.,0.,0.));
#4029=DIRECTION('center_axis',(6.12323399573676E-17,0.,1.));
#4030=DIRECTION('ref_axis',(1.,0.,0.));
#4031=DIRECTION('center_axis',(1.22464679914735E-16,-1.,0.));
#4032=DIRECTION('ref_axis',(-1.,-1.22464679914735E-16,0.));
#4033=DIRECTION('center_axis',(0.,0.,-1.));
#4034=DIRECTION('ref_axis',(1.,0.,0.));
#4035=DIRECTION('center_axis',(0.,0.,-1.));
#4036=DIRECTION('ref_axis',(1.,0.,0.));
#4037=DIRECTION('center_axis',(0.,0.,-1.));
#4038=DIRECTION('ref_axis',(-1.,0.,0.));
#4039=DIRECTION('',(-0.0871557427578718,1.06735001395738E-17,0.996194698090852));
#4935=CARTESIAN_POINT('',(0.,0.,0.));
#4936=CARTESIAN_POINT('Origin',(-1.41899999999985,1.41899999999965,3.1));
#4937=CARTESIAN_POINT('',(-1.41899999999985,0.472999999999654,3.01252522110193));
#4938=CARTESIAN_POINT('',(-0.472999999999848,1.41899999999969,3.01252522110194));
#4939=CARTESIAN_POINT('Ctrl Pts',(-1.41899999999985,0.472999999999654,3.01252522110193));
#4940=CARTESIAN_POINT('Ctrl Pts',(-1.418237843063,0.472999999999654,3.01261008153857));
#4941=CARTESIAN_POINT('Ctrl Pts',(-1.41747599318127,0.473000921064105,3.01269480438576));
#4942=CARTESIAN_POINT('Ctrl Pts',(-1.29873656917598,0.473287797471327,3.02588334070707));
#4943=CARTESIAN_POINT('Ctrl Pts',(-1.17260477262757,0.497030428020145,3.03726209636997));
#4944=CARTESIAN_POINT('Ctrl Pts',(-0.940241249793281,0.593452559529333,
3.05235989856665));
#4945=CARTESIAN_POINT('Ctrl Pts',(-0.834013199901804,0.666140770092746,
3.05607990145755));
#4946=CARTESIAN_POINT('Ctrl Pts',(-0.75007698499736,0.750076984997194,3.05607990145756));
#4947=CARTESIAN_POINT('Ctrl Pts',(-0.666140770092915,0.834013199901643,
3.05607990145756));
#4948=CARTESIAN_POINT('Ctrl Pts',(-0.593452559529506,0.940241249793123,
3.05235989856665));
#4949=CARTESIAN_POINT('Ctrl Pts',(-0.497030428020328,1.17260477262741,3.03726209636997));
#4950=CARTESIAN_POINT('Ctrl Pts',(-0.473287797471517,1.29873656917583,3.02588334070708));
#4951=CARTESIAN_POINT('Ctrl Pts',(-0.4730009210643,1.41747599318095,3.01269480438579));
#4952=CARTESIAN_POINT('Ctrl Pts',(-0.472999999999848,1.41823784306269,3.0126100815386));
#4953=CARTESIAN_POINT('Ctrl Pts',(-0.472999999999848,1.41899999999969,3.01252522110194));
#4954=CARTESIAN_POINT('',(-1.41899999999985,0.472999999999654,1.22765307701778));
#4955=CARTESIAN_POINT('',(-1.41899999999985,0.472999999999654,3.1));
#4956=CARTESIAN_POINT('',(-0.866098738193358,0.651395808574938,0.27));
#4957=CARTESIAN_POINT('Origin',(-1.41899999999985,1.41899999999965,1.22765307701778));
#4958=CARTESIAN_POINT('',(-0.651395808574991,0.86609873819336,0.27));
#4959=CARTESIAN_POINT('Origin',(-1.41899999999985,1.41899999999965,0.27));
#4960=CARTESIAN_POINT('',(-0.472999999999848,1.41899999999969,1.22765307701751));
#4961=CARTESIAN_POINT('Origin',(-1.41899999999985,1.41899999999965,1.22765307701745));
#4962=CARTESIAN_POINT('',(-0.472999999999848,1.41899999999969,3.1));
#4963=CARTESIAN_POINT('Origin',(-0.472999999999807,0.472999999999754,3.1));
#4964=CARTESIAN_POINT('',(-0.472999999999889,2.36767196216383,2.87080111520185));
#4965=CARTESIAN_POINT('Origin',(-0.472999999999787,-2.0353210154902E-14,
-9.73193776093083));
#4966=CARTESIAN_POINT('',(-0.472999999999884,2.24662499999997,2.66114162663218));
#4967=CARTESIAN_POINT('Origin',(-0.472999999999895,2.5,3.1));
#4968=CARTESIAN_POINT('',(0.472999999999787,2.36767196216383,2.87080111520185));
#4969=CARTESIAN_POINT('Origin',(1.16338464595253E-14,-3.68139204037345,
-7.60648507542867));
#4970=CARTESIAN_POINT('',(0.651395808575038,0.866098738193364,0.27));
#4971=CARTESIAN_POINT('',(-0.236499999999946,0.866098738193362,0.27));
#4972=CARTESIAN_POINT('',(0.472999999999754,1.41899999999989,1.22765307701784));
#4973=CARTESIAN_POINT('Origin',(1.41899999999975,1.41899999999985,1.22765307701778));
#4974=CARTESIAN_POINT('',(0.472999999999791,2.5,3.09999999999999));
#4975=CARTESIAN_POINT('Origin',(0.472999999999791,2.5,3.1));
#4976=CARTESIAN_POINT('',(0.472999999999754,1.41899999999989,3.01252522110192));
#4977=CARTESIAN_POINT('Origin',(0.472999999999705,-1.6370004348928E-14,
-9.73193776093083));
#4978=CARTESIAN_POINT('',(0.472999999999754,1.41899999999989,3.1));
#4979=CARTESIAN_POINT('Origin',(1.41899999999975,1.41899999999985,3.1));
#4980=CARTESIAN_POINT('',(1.41899999999979,0.472999999999854,3.01252522110193));
#4981=CARTESIAN_POINT('Ctrl Pts',(0.472999999999754,1.41899999999989,3.01252522110192));
#4982=CARTESIAN_POINT('Ctrl Pts',(0.472999999999754,1.41823784306304,3.01261008153856));
#4983=CARTESIAN_POINT('Ctrl Pts',(0.473000921064206,1.4174759931813,3.01269480438575));
#4984=CARTESIAN_POINT('Ctrl Pts',(0.473287797471426,1.29873656917601,3.02588334070706));
#4985=CARTESIAN_POINT('Ctrl Pts',(0.49703042802024,1.17260477262759,3.03726209636996));
#4986=CARTESIAN_POINT('Ctrl Pts',(0.593452559529424,0.940241249793303,3.05235989856665));
#4987=CARTESIAN_POINT('Ctrl Pts',(0.666140770092836,0.834013199901824,3.05607990145755));
#4988=CARTESIAN_POINT('Ctrl Pts',(0.750076984997282,0.750076984997378,3.05607990145755));
#4989=CARTESIAN_POINT('Ctrl Pts',(0.834013199901729,0.666140770092932,3.05607990145755));
#4990=CARTESIAN_POINT('Ctrl Pts',(0.940241249793208,0.593452559529521,3.05235989856665));
#4991=CARTESIAN_POINT('Ctrl Pts',(1.1726047726275,0.497030428020338,3.03726209636996));
#4992=CARTESIAN_POINT('Ctrl Pts',(1.29873656917591,0.473287797471525,3.02588334070707));
#4993=CARTESIAN_POINT('Ctrl Pts',(1.41747599318104,0.473000921064306,3.01269480438578));
#4994=CARTESIAN_POINT('Ctrl Pts',(1.41823784306278,0.472999999999854,3.01261008153858));
#4995=CARTESIAN_POINT('Ctrl Pts',(1.41899999999979,0.472999999999854,3.01252522110193));
#4996=CARTESIAN_POINT('',(0.866098738193361,0.651395808575069,0.27));
#4997=CARTESIAN_POINT('Origin',(1.41899999999975,1.41899999999985,0.27));
#4998=CARTESIAN_POINT('',(1.41899999999979,0.472999999999853,1.22765307701768));
#4999=CARTESIAN_POINT('Origin',(1.41899999999975,1.41899999999985,1.22765307701762));
#5000=CARTESIAN_POINT('',(1.41899999999979,0.472999999999854,3.1));
#5001=CARTESIAN_POINT('Origin',(0.472999999999817,0.472999999999815,3.1));
#5002=CARTESIAN_POINT('',(2.36767196216383,0.472999999999892,2.87080111520185));
#5003=CARTESIAN_POINT('Origin',(-1.83061508724184E-14,0.472999999999796,
-9.73193776093083));
#5004=CARTESIAN_POINT('',(2.24662499999998,0.472999999999887,2.6611416266322));
#5005=CARTESIAN_POINT('Origin',(2.5,0.472999999999897,3.1));
#5006=CARTESIAN_POINT('',(2.36767196216383,-0.472999999999786,2.87080111520185));
#5007=CARTESIAN_POINT('Origin',(-3.68139204037345,0.,-7.60648507542867));
#5008=CARTESIAN_POINT('',(0.866098738193361,-0.65139580857508,0.270000000000001));
#5009=CARTESIAN_POINT('',(0.86609873819336,0.236499999999951,0.27));
#5010=CARTESIAN_POINT('',(1.41899999999987,-0.472999999999785,1.22765307701781));
#5011=CARTESIAN_POINT('Origin',(1.41899999999987,-1.41899999999979,1.22765307701781));
#5012=CARTESIAN_POINT('',(2.5,-0.472999999999786,3.1));
#5013=CARTESIAN_POINT('Origin',(2.5,-0.472999999999786,3.1));
#5014=CARTESIAN_POINT('',(1.41899999999987,-0.472999999999785,3.01252522110192));
#5015=CARTESIAN_POINT('Origin',(6.05980759185948E-16,-0.472999999999784,
-9.73193776093083));
#5016=CARTESIAN_POINT('',(1.41899999999987,-0.472999999999785,3.1));
#5017=CARTESIAN_POINT('Origin',(-1.41899999999978,-1.41899999999983,3.1));
#5018=CARTESIAN_POINT('',(-0.472999999999784,-1.41899999999984,3.01252522110192));
#5019=CARTESIAN_POINT('',(-1.41899999999983,-0.472999999999835,3.01252522110192));
#5020=CARTESIAN_POINT('Ctrl Pts',(-0.472999999999784,-1.41899999999984,
3.01252522110192));
#5021=CARTESIAN_POINT('Ctrl Pts',(-0.472999999999784,-1.41823784306299,
3.01261008153856));
#5022=CARTESIAN_POINT('Ctrl Pts',(-0.473000921064235,-1.41747599318126,
3.01269480438576));
#5023=CARTESIAN_POINT('Ctrl Pts',(-0.473287797471458,-1.29873656917597,
3.02588334070707));
#5024=CARTESIAN_POINT('Ctrl Pts',(-0.497030428020275,-1.17260477262755,
3.03726209636996));
#5025=CARTESIAN_POINT('Ctrl Pts',(-0.593452559529464,-0.940241249793266,
3.05235989856664));
#5026=CARTESIAN_POINT('Ctrl Pts',(-0.666140770092878,-0.834013199901788,
3.05607990145755));
#5027=CARTESIAN_POINT('Ctrl Pts',(-0.750076984997327,-0.750076984997344,
3.05607990145755));
#5028=CARTESIAN_POINT('Ctrl Pts',(-0.834013199901775,-0.6661407700929,3.05607990145755));
#5029=CARTESIAN_POINT('Ctrl Pts',(-0.940241249793256,-0.593452559529491,
3.05235989856665));
#5030=CARTESIAN_POINT('Ctrl Pts',(-1.17260477262755,-0.497030428020314,
3.03726209636996));
#5031=CARTESIAN_POINT('Ctrl Pts',(-1.29873656917596,-0.473287797471503,
3.02588334070706));
#5032=CARTESIAN_POINT('Ctrl Pts',(-1.41747599318109,-0.473000921064287,
3.01269480438577));
#5033=CARTESIAN_POINT('Ctrl Pts',(-1.41823784306282,-0.472999999999835,
3.01261008153858));
#5034=CARTESIAN_POINT('Ctrl Pts',(-1.41899999999983,-0.472999999999835,
3.01252522110192));
#5035=CARTESIAN_POINT('',(-0.472999999999784,-1.41899999999984,1.22765307701777));
#5036=CARTESIAN_POINT('',(-0.472999999999784,-1.41899999999984,3.1));
#5037=CARTESIAN_POINT('',(-0.651395808575061,-0.866098738193354,0.27));
#5038=CARTESIAN_POINT('Origin',(-1.41899999999978,-1.41899999999983,1.22765307701777));
#5039=CARTESIAN_POINT('',(-0.866098738193358,-0.651395808575073,0.27));
#5040=CARTESIAN_POINT('Origin',(-1.41899999999978,-1.41899999999983,0.27));
#5041=CARTESIAN_POINT('',(-1.41899999999983,-0.472999999999835,1.22765307701776));
#5042=CARTESIAN_POINT('Origin',(-1.41899999999978,-1.41899999999983,1.22765307701767));
#5043=CARTESIAN_POINT('',(-1.41899999999983,-0.472999999999835,3.1));
#5044=CARTESIAN_POINT('Origin',(-0.472999999999781,-0.472999999999784,3.1));
#5045=CARTESIAN_POINT('',(-2.36767196216382,-0.472999999999886,2.87080111520185));
#5046=CARTESIAN_POINT('Origin',(2.61729806275939E-14,-0.472999999999759,
-9.73193776093083));
#5047=CARTESIAN_POINT('',(-2.24662499999997,-0.472999999999879,2.66114162663219));
#5048=CARTESIAN_POINT('Origin',(1.41899999999987,-1.41899999999979,3.1));
#5049=CARTESIAN_POINT('',(0.472999999999865,-1.41899999999981,3.01252522110192));
#5050=CARTESIAN_POINT('Ctrl Pts',(1.41899999999987,-0.472999999999785,3.01252522110192));
#5051=CARTESIAN_POINT('Ctrl Pts',(1.41823784306302,-0.472999999999785,3.01261008153856));
#5052=CARTESIAN_POINT('Ctrl Pts',(1.41747599318129,-0.473000921064237,3.01269480438575));
#5053=CARTESIAN_POINT('Ctrl Pts',(1.29873656917601,-0.473287797471458,3.02588334070706));
#5054=CARTESIAN_POINT('Ctrl Pts',(1.17260477262759,-0.497030428020274,3.03726209636996));
#5055=CARTESIAN_POINT('Ctrl Pts',(0.940241249793305,-0.59345255952946,3.05235989856664));
#5056=CARTESIAN_POINT('Ctrl Pts',(0.834013199901827,-0.666140770092873,
3.05607990145755));
#5057=CARTESIAN_POINT('Ctrl Pts',(0.750076984997382,-0.75007698499732,3.05607990145755));
#5058=CARTESIAN_POINT('Ctrl Pts',(0.666140770092937,-0.834013199901768,
3.05607990145755));
#5059=CARTESIAN_POINT('Ctrl Pts',(0.593452559529527,-0.940241249793248,
3.05235989856665));
#5060=CARTESIAN_POINT('Ctrl Pts',(0.497030428020347,-1.17260477262754,3.03726209636996));
#5061=CARTESIAN_POINT('Ctrl Pts',(0.473287797471535,-1.29873656917595,3.02588334070706));
#5062=CARTESIAN_POINT('Ctrl Pts',(0.473000921064317,-1.41747599318107,3.01269480438577));
#5063=CARTESIAN_POINT('Ctrl Pts',(0.472999999999865,-1.4182378430628,3.01261008153858));
#5064=CARTESIAN_POINT('Ctrl Pts',(0.472999999999865,-1.41899999999981,3.01252522110192));
#5065=CARTESIAN_POINT('',(0.651395808575106,-0.866098738193356,0.27));
#5066=CARTESIAN_POINT('Origin',(1.41899999999987,-1.41899999999979,0.27));
#5067=CARTESIAN_POINT('',(0.472999999999865,-1.41899999999981,1.22765307701772));
#5068=CARTESIAN_POINT('Origin',(1.41899999999987,-1.41899999999979,1.22765307701768));
#5069=CARTESIAN_POINT('',(0.472999999999865,-1.41899999999981,3.1));
#5070=CARTESIAN_POINT('Origin',(0.472999999999839,-0.472999999999785,3.1));
#5071=CARTESIAN_POINT('',(0.472999999999892,-2.36767196216382,2.87080111520185));
#5072=CARTESIAN_POINT('Origin',(0.472999999999825,1.32935445800918E-14,
-9.73193776093083));
#5073=CARTESIAN_POINT('',(0.472999999999889,-2.24662499999997,2.66114162663219));
#5074=CARTESIAN_POINT('Origin',(-2.5,0.472999999999654,3.1));
#5075=CARTESIAN_POINT('',(-2.36767196216383,0.472999999999654,2.87080111520186));
#5076=CARTESIAN_POINT('Origin',(8.32667268468867E-16,0.472999999999654,
-9.73193776093083));
#5077=CARTESIAN_POINT('',(-2.5,0.472999999999654,3.1));
#5078=CARTESIAN_POINT('Origin',(-2.5,-0.472999999999893,3.1));
#5079=CARTESIAN_POINT('',(-2.37229341204248,-2.90522153369617E-16,2.87880570119631));
#5080=CARTESIAN_POINT('Origin',(3.68139204037345,0.,-7.60648507542867));
#5081=CARTESIAN_POINT('',(-0.866098738193358,-0.236499999999945,0.27));
#5082=CARTESIAN_POINT('Origin',(3.68139204037345,0.,-7.60648507542867));
#5083=CARTESIAN_POINT('Origin',(-0.472999999999788,-2.5,3.1));
#5084=CARTESIAN_POINT('',(-0.472999999999788,-2.36767196216382,2.87080111520185));
#5085=CARTESIAN_POINT('Origin',(-0.472999999999779,1.82968396778355E-15,
-9.73193776093083));
#5086=CARTESIAN_POINT('',(-0.472999999999788,-2.5,3.1));
#5087=CARTESIAN_POINT('Origin',(0.472999999999896,-2.5,3.1));
#5088=CARTESIAN_POINT('Origin',(6.23325686399709E-15,3.68139204037346,-7.60648507542867));
#5089=CARTESIAN_POINT('',(0.236499999999949,-0.866098738193356,0.27));
#5090=CARTESIAN_POINT('Origin',(1.11022302462516E-15,3.88578058618805E-15,
0.27));
#5091=CARTESIAN_POINT('Origin',(0.,0.,-0.2));
#5092=CARTESIAN_POINT('',(2.37846096908266,-2.91277461268399E-16,-3.46944695195361E-17));
#5093=CARTESIAN_POINT('Origin',(0.,0.,-3.46944695195361E-17));
#5094=CARTESIAN_POINT('',(2.17846096908266,-2.66784525285452E-16,-0.2));
#5095=CARTESIAN_POINT('Origin',(2.37846096908266,-2.91277461268399E-16,
-0.2));
#5096=CARTESIAN_POINT('Origin',(0.,0.,-0.2));
#5097=CARTESIAN_POINT('Origin',(-2.17846096908266,0.,-1.88141750998334E-17));
#5098=CARTESIAN_POINT('',(5.15,-6.30693101560887E-16,-2.77555756156289E-16));
#5099=CARTESIAN_POINT('Origin',(0.,0.,0.));
#5100=CARTESIAN_POINT('Origin',(0.,0.,-0.149999999999999));
#5101=CARTESIAN_POINT('',(2.17846096908266,-2.66784525285452E-16,-0.299999999999998));
#5102=CARTESIAN_POINT('Origin',(0.,0.,-0.299999999999998));
#5103=CARTESIAN_POINT('',(2.17846096908266,-2.66784525285452E-16,-0.149999999999999));
#5104=CARTESIAN_POINT('Origin',(0.,0.,-0.899999999999999));
#5105=CARTESIAN_POINT('',(2.4505,-3.00099698131059E-16,-1.31526348502534));
#5106=CARTESIAN_POINT('Origin',(0.,0.,-1.31526348502534));
#5107=CARTESIAN_POINT('',(2.33923048454133,-2.86473112536145E-16,-0.899999999999999));
#5108=CARTESIAN_POINT('Origin',(0.,0.,-7.75));
#5109=CARTESIAN_POINT('',(2.4505,3.00099698131059E-16,-14.));
#5110=CARTESIAN_POINT('Origin',(0.,0.,-14.));
#5111=CARTESIAN_POINT('',(2.4505,-3.00099698131059E-16,-7.75));
#5112=CARTESIAN_POINT('Origin',(0.,0.,-14.));
#5113=CARTESIAN_POINT('Origin',(8.32667268468867E-16,0.,-9.73193776093083));
#5114=CARTESIAN_POINT('',(-4.96627380657387,0.,2.1));
#5115=CARTESIAN_POINT('Origin',(8.32667268468867E-16,0.,-9.73193776093083));
#5116=CARTESIAN_POINT('',(4.96627380657386,-6.08193132091002E-16,2.1));
#5117=CARTESIAN_POINT('Origin',(0.,0.,2.1));
#5118=CARTESIAN_POINT('Origin',(0.,0.,2.1));
#5119=CARTESIAN_POINT('Origin',(0.,0.,1.05));
#5120=CARTESIAN_POINT('',(5.05813690328693,-6.19443116825945E-16,1.05));
#7025=UNCERTAINTY_MEASURE_WITH_UNIT(LENGTH_MEASURE(0.01),#7048,
'DISTANCE_ACCURACY_VALUE',
'Maximum model space distance between geometric entities at asserted c
onnectivities');
#7035=UNCERTAINTY_MEASURE_WITH_UNIT(LENGTH_MEASURE(0.01),#7048,
'DISTANCE_ACCURACY_VALUE',
'Maximum model space distance between geometric entities at asserted c
onnectivities');
#7037=(
GEOMETRIC_REPRESENTATION_CONTEXT(3)
GLOBAL_UNCERTAINTY_ASSIGNED_CONTEXT((#7025))
GLOBAL_UNIT_ASSIGNED_CONTEXT((#7048,#7050,#7051))
REPRESENTATION_CONTEXT('','3D')
);
#7047=(
GEOMETRIC_REPRESENTATION_CONTEXT(3)
GLOBAL_UNCERTAINTY_ASSIGNED_CONTEXT((#7035))
GLOBAL_UNIT_ASSIGNED_CONTEXT((#7048,#7050,#7051))
REPRESENTATION_CONTEXT('','3D')
);
#7048=(
LENGTH_UNIT()
NAMED_UNIT(*)
SI_UNIT(.MILLI.,.METRE.)
);
#7050=(
NAMED_UNIT(*)
PLANE_ANGLE_UNIT()
SI_UNIT($,.RADIAN.)
);
#7051=(
NAMED_UNIT(*)
SI_UNIT($,.STERADIAN.)
SOLID_ANGLE_UNIT()
);
#7053=SHAPE_DEFINITION_REPRESENTATION(#7064,#7085);
#7064=PRODUCT_DEFINITION_SHAPE('',$,#7097);
#7085=SHAPE_REPRESENTATION('',(#3519),#7037);
#7095=PRODUCT_DEFINITION_CONTEXT('part definition',#7130,'design');
#7097=PRODUCT_DEFINITION('BHS JIS B 1111 - M5x14 Steel 4.6 Plain',
'M5x14 Steel 4.6 Plain v1',#7108,#7095);
#7108=PRODUCT_DEFINITION_FORMATION('',$,#7133);
#7130=APPLICATION_CONTEXT(
'Core Data for Automotive Mechanical Design Process');
#7131=PRODUCT_CONTEXT('part definition',#7130,'mechanical');
#7133=PRODUCT('BHS JIS B 1111 - M5x14 Steel 4.6 Plain',
'M5x14 Steel 4.6 Plain v1','Binding Head Screw JIS B 1111 - M5x14',(#7131));
#7206=COLOUR_RGB('Off White',0.89,0.88,0.83);
#7207=FILL_AREA_STYLE_COLOUR('',#7206);
#7208=FILL_AREA_STYLE('',(#7207));
#7209=SURFACE_STYLE_FILL_AREA(#7208);
#7210=SURFACE_SIDE_STYLE('',(#7209));
#7211=SURFACE_STYLE_USAGE(.BOTH.,#7210);
#7212=PRESENTATION_STYLE_ASSIGNMENT((#7211));
ENDSEC;
END-ISO-10303-21;
